ISO-10303-21;
HEADER;
/* Generated by software containing ST-Developer
 * from STEP Tools, Inc. (www.steptools.com) 
 */

FILE_DESCRIPTION(
/* description */ ('Bell-crank linkage with push rods'),
/* implementation_level */ '2;1');

FILE_NAME(
/* name */ 'Upper pin sleeve (3).step',
/* time_stamp */ '2026-10-28T03:25:15-07:00',
/* author */ (''),
/* organization */ (''),
/* preprocessor_version */ 'ST-DEVELOPER v20.2',
/* originating_system */ 'Autodesk Translation Framework v15.17.0.0',
/* authorisation */ '');

FILE_SCHEMA (('AUTOMOTIVE_DESIGN { 1 0 10303 214 3 1 1 }'));
ENDSEC;

DATA;
#10=MECHANICAL_DESIGN_GEOMETRIC_PRESENTATION_REPRESENTATION('',(#661),#16678);
#545=SHAPE_REPRESENTATION_RELATIONSHIP('SRR','None',#16967,#599);
#599=ADVANCED_BREP_SHAPE_REPRESENTATION('',(#721),#16672);
#661=STYLED_ITEM('',(#17291),#721);
#721=MANIFOLD_SOLID_BREP('Body1',#8853);
#950=FACE_BOUND('',#2470,.T.);
#951=FACE_BOUND('',#2472,.T.);
#1215=PLANE('',#10455);
#1216=PLANE('',#10456);
#1720=FACE_OUTER_BOUND('',#2467,.T.);
#1721=FACE_OUTER_BOUND('',#2468,.T.);
#1722=FACE_OUTER_BOUND('',#2469,.T.);
#1723=FACE_OUTER_BOUND('',#2471,.T.);
#2467=EDGE_LOOP('',(#7887,#7888,#7889,#7890));
#2468=EDGE_LOOP('',(#7891,#7892,#7893,#7894));
#2469=EDGE_LOOP('',(#7895));
#2470=EDGE_LOOP('',(#7896));
#2471=EDGE_LOOP('',(#7897));
#2472=EDGE_LOOP('',(#7898));
#3028=LINE('',#16262,#3577);
#3029=LINE('',#16268,#3578);
#3577=VECTOR('',#13120,0.305);
#3578=VECTOR('',#13127,0.5);
#4083=CIRCLE('',#10450,0.305);
#4084=CIRCLE('',#10451,0.305);
#4085=CIRCLE('',#10453,0.5);
#4086=CIRCLE('',#10454,0.5);
#4774=VERTEX_POINT('',#16259);
#4775=VERTEX_POINT('',#16261);
#4776=VERTEX_POINT('',#16265);
#4777=VERTEX_POINT('',#16267);
#5821=EDGE_CURVE('',#4774,#4774,#4083,.T.);
#5822=EDGE_CURVE('',#4774,#4775,#3028,.T.);
#5823=EDGE_CURVE('',#4775,#4775,#4084,.T.);
#5824=EDGE_CURVE('',#4776,#4776,#4085,.T.);
#5825=EDGE_CURVE('',#4776,#4777,#3029,.T.);
#5826=EDGE_CURVE('',#4777,#4777,#4086,.T.);
#7887=ORIENTED_EDGE('',*,*,#5821,.F.);
#7888=ORIENTED_EDGE('',*,*,#5822,.T.);
#7889=ORIENTED_EDGE('',*,*,#5823,.T.);
#7890=ORIENTED_EDGE('',*,*,#5822,.F.);
#7891=ORIENTED_EDGE('',*,*,#5824,.F.);
#7892=ORIENTED_EDGE('',*,*,#5825,.T.);
#7893=ORIENTED_EDGE('',*,*,#5826,.T.);
#7894=ORIENTED_EDGE('',*,*,#5825,.F.);
#7895=ORIENTED_EDGE('',*,*,#5824,.T.);
#7896=ORIENTED_EDGE('',*,*,#5821,.T.);
#7897=ORIENTED_EDGE('',*,*,#5826,.F.);
#7898=ORIENTED_EDGE('',*,*,#5823,.F.);
#8258=CYLINDRICAL_SURFACE('',#10449,0.305);
#8259=CYLINDRICAL_SURFACE('',#10452,0.5);
#8745=ADVANCED_FACE('',(#1720),#8258,.F.);
#8746=ADVANCED_FACE('',(#1721),#8259,.T.);
#8747=ADVANCED_FACE('',(#1722,#950),#1215,.T.);
#8748=ADVANCED_FACE('',(#1723,#951),#1216,.F.);
#8853=CLOSED_SHELL('',(#8745,#8746,#8747,#8748));
#10448=AXIS2_PLACEMENT_3D('',#16257,#13114,#13115);
#10449=AXIS2_PLACEMENT_3D('',#16258,#13116,#13117);
#10450=AXIS2_PLACEMENT_3D('',#16260,#13118,#13119);
#10451=AXIS2_PLACEMENT_3D('',#16263,#13121,#13122);
#10452=AXIS2_PLACEMENT_3D('',#16264,#13123,#13124);
#10453=AXIS2_PLACEMENT_3D('',#16266,#13125,#13126);
#10454=AXIS2_PLACEMENT_3D('',#16269,#13128,#13129);
#10455=AXIS2_PLACEMENT_3D('',#16270,#13130,#13131);
#10456=AXIS2_PLACEMENT_3D('',#16271,#13132,#13133);
#13114=DIRECTION('axis',(0.,0.,1.));
#13115=DIRECTION('refdir',(1.,0.,0.));
#13116=DIRECTION('center_axis',(0.,0.,1.));
#13117=DIRECTION('ref_axis',(1.,0.,0.));
#13118=DIRECTION('center_axis',(0.,0.,-1.));
#13119=DIRECTION('ref_axis',(1.,0.,0.));
#13120=DIRECTION('',(0.,0.,-1.));
#13121=DIRECTION('center_axis',(0.,0.,-1.));
#13122=DIRECTION('ref_axis',(1.,0.,0.));
#13123=DIRECTION('center_axis',(0.,0.,1.));
#13124=DIRECTION('ref_axis',(1.,0.,0.));
#13125=DIRECTION('center_axis',(0.,0.,1.));
#13126=DIRECTION('ref_axis',(1.,0.,0.));
#13127=DIRECTION('',(0.,0.,-1.));
#13128=DIRECTION('center_axis',(0.,0.,1.));
#13129=DIRECTION('ref_axis',(1.,0.,0.));
#13130=DIRECTION('center_axis',(0.,0.,1.));
#13131=DIRECTION('ref_axis',(1.,0.,0.));
#13132=DIRECTION('center_axis',(0.,0.,1.));
#13133=DIRECTION('ref_axis',(1.,0.,0.));
#16257=CARTESIAN_POINT('',(0.,0.,0.));
#16258=CARTESIAN_POINT('Origin',(4.,12.,7.6));
#16259=CARTESIAN_POINT('',(3.695,12.,8.1));
#16260=CARTESIAN_POINT('Origin',(4.,12.,8.1));
#16261=CARTESIAN_POINT('',(3.695,12.,7.6));
#16262=CARTESIAN_POINT('',(3.695,12.,7.6));
#16263=CARTESIAN_POINT('Origin',(4.,12.,7.6));
#16264=CARTESIAN_POINT('Origin',(4.,12.,7.6));
#16265=CARTESIAN_POINT('',(3.5,12.,8.1));
#16266=CARTESIAN_POINT('Origin',(4.,12.,8.1));
#16267=CARTESIAN_POINT('',(3.5,12.,7.6));
#16268=CARTESIAN_POINT('',(3.5,12.,7.6));
#16269=CARTESIAN_POINT('Origin',(4.,12.,7.6));
#16270=CARTESIAN_POINT('Origin',(4.,12.,8.1));
#16271=CARTESIAN_POINT('Origin',(4.,12.,7.6));
#16608=UNCERTAINTY_MEASURE_WITH_UNIT(LENGTH_MEASURE(0.001),#16679,
'DISTANCE_ACCURACY_VALUE',
'Maximum model space distance between geometric entities at asserted c
onnectivities');
#16614=UNCERTAINTY_MEASURE_WITH_UNIT(LENGTH_MEASURE(0.001),#16679,
'DISTANCE_ACCURACY_VALUE',
'Maximum model space distance between geometric entities at asserted c
onnectivities');
#16672=(
GEOMETRIC_REPRESENTATION_CONTEXT(3)
GLOBAL_UNCERTAINTY_ASSIGNED_CONTEXT((#16608))
GLOBAL_UNIT_ASSIGNED_CONTEXT((#16679,#16681,#16682))
REPRESENTATION_CONTEXT('','3D')
);
#16678=(
GEOMETRIC_REPRESENTATION_CONTEXT(3)
GLOBAL_UNCERTAINTY_ASSIGNED_CONTEXT((#16614))
GLOBAL_UNIT_ASSIGNED_CONTEXT((#16679,#16681,#16682))
REPRESENTATION_CONTEXT('','3D')
);
#16679=(
LENGTH_UNIT()
NAMED_UNIT(*)
SI_UNIT(.CENTI.,.METRE.)
);
#16681=(
NAMED_UNIT(*)
PLANE_ANGLE_UNIT()
SI_UNIT($,.RADIAN.)
);
#16682=(
NAMED_UNIT(*)
SI_UNIT($,.STERADIAN.)
SOLID_ANGLE_UNIT()
);
#16740=SHAPE_DEFINITION_REPRESENTATION(#16814,#16967);
#16814=PRODUCT_DEFINITION_SHAPE('',$,#17031);
#16967=SHAPE_REPRESENTATION('',(#10448),#16672);
#16973=PRODUCT_DEFINITION_CONTEXT('part definition',#17164,'design');
#17031=PRODUCT_DEFINITION('Upper pin sleeve (3)','Upper pin sleeve (3)',#17094,
#16973);
#17094=PRODUCT_DEFINITION_FORMATION('',$,#17223);
#17164=APPLICATION_CONTEXT(
'Core Data for Automotive Mechanical Design Process');
#17165=PRODUCT_CONTEXT('part definition',#17164,'mechanical');
#17223=PRODUCT('Upper pin sleeve (3)','Upper pin sleeve (3)',
'Upper pin sleeve (3)',(#17165));
#17285=COLOUR_RGB('Grey',0.48,0.52,0.57);
#17286=FILL_AREA_STYLE_COLOUR('',#17285);
#17287=FILL_AREA_STYLE('',(#17286));
#17288=SURFACE_STYLE_FILL_AREA(#17287);
#17289=SURFACE_SIDE_STYLE('',(#17288));
#17290=SURFACE_STYLE_USAGE(.BOTH.,#17289);
#17291=PRESENTATION_STYLE_ASSIGNMENT((#17290));
ENDSEC;
END-ISO-10303-21;
